ISO-10303-21;
HEADER;
/* Generated by software containing ST-Developer
 * from STEP Tools, Inc. (www.steptools.com) 
 */

FILE_DESCRIPTION(
/* description */ ('Belt tensioner idler arm'),
/* implementation_level */ '2;1');

FILE_NAME(
/* name */ 'M4x7 cap screw.step',
/* time_stamp */ '2026-10-28T03:22:15-07:00',
/* author */ (''),
/* organization */ (''),
/* preprocessor_version */ 'ST-DEVELOPER v20.2',
/* originating_system */ 'Autodesk Translation Framework v15.17.0.0',
/* authorisation */ '');

FILE_SCHEMA (('AUTOMOTIVE_DESIGN { 1 0 10303 214 3 1 1 }'));
ENDSEC;

DATA;
#10=MECHANICAL_DESIGN_GEOMETRIC_PRESENTATION_REPRESENTATION('',(#478),#12779);
#287=ORIENTED_CLOSED_SHELL('',*,#6215,.F.);
#291=BREP_WITH_VOIDS('Body1',#6214,(#287));
#308=CONICAL_SURFACE('',#7105,0.325,0.785398163397448);
#309=CONICAL_SURFACE('',#7109,0.335,0.785398163397448);
#310=CONICAL_SURFACE('',#7113,0.21,0.463647609000806);
#402=SHAPE_REPRESENTATION_RELATIONSHIP('SRR','None',#12950,#436);
#436=ADVANCED_BREP_SHAPE_REPRESENTATION('',(#291),#12767);
#478=STYLED_ITEM('',(#13191),#291);
#636=FACE_BOUND('',#1556,.T.);
#782=PLANE('',#7101);
#783=PLANE('',#7103);
#784=PLANE('',#7111);
#785=PLANE('',#7116);
#786=PLANE('',#7117);
#787=PLANE('',#7118);
#788=PLANE('',#7119);
#789=PLANE('',#7120);
#790=PLANE('',#7121);
#791=PLANE('',#7122);
#792=PLANE('',#7123);
#1074=FACE_OUTER_BOUND('',#1550,.T.);
#1075=FACE_OUTER_BOUND('',#1551,.T.);
#1076=FACE_OUTER_BOUND('',#1552,.T.);
#1077=FACE_OUTER_BOUND('',#1553,.T.);
#1078=FACE_OUTER_BOUND('',#1554,.T.);
#1079=FACE_OUTER_BOUND('',#1555,.T.);
#1080=FACE_OUTER_BOUND('',#1557,.T.);
#1081=FACE_OUTER_BOUND('',#1558,.T.);
#1082=FACE_OUTER_BOUND('',#1559,.T.);
#1083=FACE_OUTER_BOUND('',#1560,.T.);
#1084=FACE_OUTER_BOUND('',#1561,.T.);
#1085=FACE_OUTER_BOUND('',#1562,.T.);
#1086=FACE_OUTER_BOUND('',#1563,.T.);
#1087=FACE_OUTER_BOUND('',#1564,.T.);
#1088=FACE_OUTER_BOUND('',#1565,.T.);
#1089=FACE_OUTER_BOUND('',#1566,.T.);
#1550=EDGE_LOOP('',(#5072));
#1551=EDGE_LOOP('',(#5073));
#1552=EDGE_LOOP('',(#5074,#5075,#5076,#5077));
#1553=EDGE_LOOP('',(#5078,#5079,#5080,#5081));
#1554=EDGE_LOOP('',(#5082,#5083,#5084,#5085));
#1555=EDGE_LOOP('',(#5086));
#1556=EDGE_LOOP('',(#5087));
#1557=EDGE_LOOP('',(#5088,#5089,#5090,#5091));
#1558=EDGE_LOOP('',(#5092,#5093,#5094,#5095));
#1559=EDGE_LOOP('',(#5096,#5097,#5098,#5099));
#1560=EDGE_LOOP('',(#5100,#5101,#5102,#5103));
#1561=EDGE_LOOP('',(#5104,#5105,#5106,#5107));
#1562=EDGE_LOOP('',(#5108,#5109,#5110,#5111));
#1563=EDGE_LOOP('',(#5112,#5113,#5114,#5115));
#1564=EDGE_LOOP('',(#5116,#5117,#5118,#5119));
#1565=EDGE_LOOP('',(#5120,#5121,#5122,#5123,#5124,#5125));
#1566=EDGE_LOOP('',(#5126,#5127,#5128,#5129,#5130,#5131));
#1923=LINE('',#11680,#2272);
#1924=LINE('',#11684,#2273);
#1925=LINE('',#11688,#2274);
#1926=LINE('',#11695,#2275);
#1927=LINE('',#11697,#2276);
#1928=LINE('',#11701,#2277);
#1929=LINE('',#11703,#2278);
#1930=LINE('',#11705,#2279);
#1931=LINE('',#11706,#2280);
#1932=LINE('',#11709,#2281);
#1933=LINE('',#11711,#2282);
#1934=LINE('',#11712,#2283);
#1935=LINE('',#11715,#2284);
#1936=LINE('',#11717,#2285);
#1937=LINE('',#11718,#2286);
#1938=LINE('',#11721,#2287);
#1939=LINE('',#11723,#2288);
#1940=LINE('',#11724,#2289);
#1941=LINE('',#11727,#2290);
#1942=LINE('',#11729,#2291);
#1943=LINE('',#11730,#2292);
#1944=LINE('',#11732,#2293);
#1945=LINE('',#11733,#2294);
#2272=VECTOR('',#8659,0.325);
#2273=VECTOR('',#8664,0.35);
#2274=VECTOR('',#8669,0.335);
#2275=VECTOR('',#8678,0.21);
#2276=VECTOR('',#8681,0.2);
#2277=VECTOR('',#8684,1.);
#2278=VECTOR('',#8685,1.);
#2279=VECTOR('',#8686,1.);
#2280=VECTOR('',#8687,1.);
#2281=VECTOR('',#8690,1.);
#2282=VECTOR('',#8691,1.);
#2283=VECTOR('',#8692,1.);
#2284=VECTOR('',#8695,1.);
#2285=VECTOR('',#8696,1.);
#2286=VECTOR('',#8697,1.);
#2287=VECTOR('',#8700,1.);
#2288=VECTOR('',#8701,1.);
#2289=VECTOR('',#8702,1.);
#2290=VECTOR('',#8705,1.);
#2291=VECTOR('',#8706,1.);
#2292=VECTOR('',#8707,1.);
#2293=VECTOR('',#8710,1.);
#2294=VECTOR('',#8711,1.);
#2634=CIRCLE('',#7102,0.1954);
#2635=CIRCLE('',#7104,0.3);
#2636=CIRCLE('',#7106,0.35);
#2637=CIRCLE('',#7108,0.35);
#2638=CIRCLE('',#7110,0.32);
#2639=CIRCLE('',#7112,0.22);
#2640=CIRCLE('',#7114,0.1954);
#3100=VERTEX_POINT('',#11672);
#3101=VERTEX_POINT('',#11675);
#3102=VERTEX_POINT('',#11678);
#3103=VERTEX_POINT('',#11682);
#3104=VERTEX_POINT('',#11686);
#3105=VERTEX_POINT('',#11690);
#3106=VERTEX_POINT('',#11693);
#3107=VERTEX_POINT('',#11699);
#3108=VERTEX_POINT('',#11700);
#3109=VERTEX_POINT('',#11702);
#3110=VERTEX_POINT('',#11704);
#3111=VERTEX_POINT('',#11708);
#3112=VERTEX_POINT('',#11710);
#3113=VERTEX_POINT('',#11714);
#3114=VERTEX_POINT('',#11716);
#3115=VERTEX_POINT('',#11720);
#3116=VERTEX_POINT('',#11722);
#3117=VERTEX_POINT('',#11726);
#3118=VERTEX_POINT('',#11728);
#3791=EDGE_CURVE('',#3100,#3100,#2634,.T.);
#3792=EDGE_CURVE('',#3101,#3101,#2635,.T.);
#3793=EDGE_CURVE('',#3102,#3102,#2636,.T.);
#3794=EDGE_CURVE('',#3102,#3101,#1923,.T.);
#3795=EDGE_CURVE('',#3103,#3103,#2637,.T.);
#3796=EDGE_CURVE('',#3103,#3102,#1924,.T.);
#3797=EDGE_CURVE('',#3104,#3104,#2638,.T.);
#3798=EDGE_CURVE('',#3104,#3103,#1925,.T.);
#3799=EDGE_CURVE('',#3105,#3105,#2639,.T.);
#3800=EDGE_CURVE('',#3106,#3106,#2640,.F.);
#3801=EDGE_CURVE('',#3106,#3105,#1926,.T.);
#3802=EDGE_CURVE('',#3100,#3106,#1927,.T.);
#3803=EDGE_CURVE('',#3107,#3108,#1928,.T.);
#3804=EDGE_CURVE('',#3108,#3109,#1929,.T.);
#3805=EDGE_CURVE('',#3109,#3110,#1930,.T.);
#3806=EDGE_CURVE('',#3107,#3110,#1931,.T.);
#3807=EDGE_CURVE('',#3108,#3111,#1932,.T.);
#3808=EDGE_CURVE('',#3111,#3112,#1933,.T.);
#3809=EDGE_CURVE('',#3112,#3109,#1934,.T.);
#3810=EDGE_CURVE('',#3111,#3113,#1935,.T.);
#3811=EDGE_CURVE('',#3113,#3114,#1936,.T.);
#3812=EDGE_CURVE('',#3114,#3112,#1937,.T.);
#3813=EDGE_CURVE('',#3113,#3115,#1938,.T.);
#3814=EDGE_CURVE('',#3115,#3116,#1939,.T.);
#3815=EDGE_CURVE('',#3116,#3114,#1940,.T.);
#3816=EDGE_CURVE('',#3115,#3117,#1941,.T.);
#3817=EDGE_CURVE('',#3117,#3118,#1942,.T.);
#3818=EDGE_CURVE('',#3118,#3116,#1943,.T.);
#3819=EDGE_CURVE('',#3117,#3107,#1944,.T.);
#3820=EDGE_CURVE('',#3110,#3118,#1945,.T.);
#5072=ORIENTED_EDGE('',*,*,#3791,.F.);
#5073=ORIENTED_EDGE('',*,*,#3792,.F.);
#5074=ORIENTED_EDGE('',*,*,#3793,.F.);
#5075=ORIENTED_EDGE('',*,*,#3794,.T.);
#5076=ORIENTED_EDGE('',*,*,#3792,.T.);
#5077=ORIENTED_EDGE('',*,*,#3794,.F.);
#5078=ORIENTED_EDGE('',*,*,#3795,.F.);
#5079=ORIENTED_EDGE('',*,*,#3796,.T.);
#5080=ORIENTED_EDGE('',*,*,#3793,.T.);
#5081=ORIENTED_EDGE('',*,*,#3796,.F.);
#5082=ORIENTED_EDGE('',*,*,#3797,.F.);
#5083=ORIENTED_EDGE('',*,*,#3798,.T.);
#5084=ORIENTED_EDGE('',*,*,#3795,.T.);
#5085=ORIENTED_EDGE('',*,*,#3798,.F.);
#5086=ORIENTED_EDGE('',*,*,#3797,.T.);
#5087=ORIENTED_EDGE('',*,*,#3799,.F.);
#5088=ORIENTED_EDGE('',*,*,#3800,.F.);
#5089=ORIENTED_EDGE('',*,*,#3801,.T.);
#5090=ORIENTED_EDGE('',*,*,#3799,.T.);
#5091=ORIENTED_EDGE('',*,*,#3801,.F.);
#5092=ORIENTED_EDGE('',*,*,#3791,.T.);
#5093=ORIENTED_EDGE('',*,*,#3802,.T.);
#5094=ORIENTED_EDGE('',*,*,#3800,.T.);
#5095=ORIENTED_EDGE('',*,*,#3802,.F.);
#5096=ORIENTED_EDGE('',*,*,#3803,.T.);
#5097=ORIENTED_EDGE('',*,*,#3804,.T.);
#5098=ORIENTED_EDGE('',*,*,#3805,.T.);
#5099=ORIENTED_EDGE('',*,*,#3806,.F.);
#5100=ORIENTED_EDGE('',*,*,#3807,.T.);
#5101=ORIENTED_EDGE('',*,*,#3808,.T.);
#5102=ORIENTED_EDGE('',*,*,#3809,.T.);
#5103=ORIENTED_EDGE('',*,*,#3804,.F.);
#5104=ORIENTED_EDGE('',*,*,#3810,.T.);
#5105=ORIENTED_EDGE('',*,*,#3811,.T.);
#5106=ORIENTED_EDGE('',*,*,#3812,.T.);
#5107=ORIENTED_EDGE('',*,*,#3808,.F.);
#5108=ORIENTED_EDGE('',*,*,#3813,.T.);
#5109=ORIENTED_EDGE('',*,*,#3814,.T.);
#5110=ORIENTED_EDGE('',*,*,#3815,.T.);
#5111=ORIENTED_EDGE('',*,*,#3811,.F.);
#5112=ORIENTED_EDGE('',*,*,#3816,.T.);
#5113=ORIENTED_EDGE('',*,*,#3817,.T.);
#5114=ORIENTED_EDGE('',*,*,#3818,.T.);
#5115=ORIENTED_EDGE('',*,*,#3814,.F.);
#5116=ORIENTED_EDGE('',*,*,#3819,.T.);
#5117=ORIENTED_EDGE('',*,*,#3806,.T.);
#5118=ORIENTED_EDGE('',*,*,#3820,.T.);
#5119=ORIENTED_EDGE('',*,*,#3817,.F.);
#5120=ORIENTED_EDGE('',*,*,#3819,.F.);
#5121=ORIENTED_EDGE('',*,*,#3816,.F.);
#5122=ORIENTED_EDGE('',*,*,#3813,.F.);
#5123=ORIENTED_EDGE('',*,*,#3810,.F.);
#5124=ORIENTED_EDGE('',*,*,#3807,.F.);
#5125=ORIENTED_EDGE('',*,*,#3803,.F.);
#5126=ORIENTED_EDGE('',*,*,#3820,.F.);
#5127=ORIENTED_EDGE('',*,*,#3805,.F.);
#5128=ORIENTED_EDGE('',*,*,#3809,.F.);
#5129=ORIENTED_EDGE('',*,*,#3812,.F.);
#5130=ORIENTED_EDGE('',*,*,#3815,.F.);
#5131=ORIENTED_EDGE('',*,*,#3818,.F.);
#5746=CYLINDRICAL_SURFACE('',#7107,0.35);
#5747=CYLINDRICAL_SURFACE('',#7115,0.1954);
#6051=ADVANCED_FACE('',(#1074),#782,.F.);
#6052=ADVANCED_FACE('',(#1075),#783,.T.);
#6053=ADVANCED_FACE('',(#1076),#308,.T.);
#6054=ADVANCED_FACE('',(#1077),#5746,.T.);
#6055=ADVANCED_FACE('',(#1078),#309,.T.);
#6056=ADVANCED_FACE('',(#1079,#636),#784,.T.);
#6057=ADVANCED_FACE('',(#1080),#310,.T.);
#6058=ADVANCED_FACE('',(#1081),#5747,.T.);
#6059=ADVANCED_FACE('',(#1082),#785,.F.);
#6060=ADVANCED_FACE('',(#1083),#786,.F.);
#6061=ADVANCED_FACE('',(#1084),#787,.F.);
#6062=ADVANCED_FACE('',(#1085),#788,.F.);
#6063=ADVANCED_FACE('',(#1086),#789,.F.);
#6064=ADVANCED_FACE('',(#1087),#790,.F.);
#6065=ADVANCED_FACE('',(#1088),#791,.F.);
#6066=ADVANCED_FACE('',(#1089),#792,.F.);
#6214=CLOSED_SHELL('',(#6051,#6052,#6053,#6054,#6055,#6056,#6057,#6058));
#6215=CLOSED_SHELL('',(#6059,#6060,#6061,#6062,#6063,#6064,#6065,#6066));
#7100=AXIS2_PLACEMENT_3D('',#11670,#8645,#8646);
#7101=AXIS2_PLACEMENT_3D('',#11671,#8647,#8648);
#7102=AXIS2_PLACEMENT_3D('',#11673,#8649,#8650);
#7103=AXIS2_PLACEMENT_3D('',#11674,#8651,#8652);
#7104=AXIS2_PLACEMENT_3D('',#11676,#8653,#8654);
#7105=AXIS2_PLACEMENT_3D('',#11677,#8655,#8656);
#7106=AXIS2_PLACEMENT_3D('',#11679,#8657,#8658);
#7107=AXIS2_PLACEMENT_3D('',#11681,#8660,#8661);
#7108=AXIS2_PLACEMENT_3D('',#11683,#8662,#8663);
#7109=AXIS2_PLACEMENT_3D('',#11685,#8665,#8666);
#7110=AXIS2_PLACEMENT_3D('',#11687,#8667,#8668);
#7111=AXIS2_PLACEMENT_3D('',#11689,#8670,#8671);
#7112=AXIS2_PLACEMENT_3D('',#11691,#8672,#8673);
#7113=AXIS2_PLACEMENT_3D('',#11692,#8674,#8675);
#7114=AXIS2_PLACEMENT_3D('',#11694,#8676,#8677);
#7115=AXIS2_PLACEMENT_3D('',#11696,#8679,#8680);
#7116=AXIS2_PLACEMENT_3D('',#11698,#8682,#8683);
#7117=AXIS2_PLACEMENT_3D('',#11707,#8688,#8689);
#7118=AXIS2_PLACEMENT_3D('',#11713,#8693,#8694);
#7119=AXIS2_PLACEMENT_3D('',#11719,#8698,#8699);
#7120=AXIS2_PLACEMENT_3D('',#11725,#8703,#8704);
#7121=AXIS2_PLACEMENT_3D('',#11731,#8708,#8709);
#7122=AXIS2_PLACEMENT_3D('',#11734,#8712,#8713);
#7123=AXIS2_PLACEMENT_3D('',#11735,#8714,#8715);
#8645=DIRECTION('axis',(0.,0.,1.));
#8646=DIRECTION('refdir',(1.,0.,0.));
#8647=DIRECTION('center_axis',(0.,1.,0.));
#8648=DIRECTION('ref_axis',(1.,0.,0.));
#8649=DIRECTION('center_axis',(0.,1.,0.));
#8650=DIRECTION('ref_axis',(1.,0.,0.));
#8651=DIRECTION('center_axis',(0.,1.,0.));
#8652=DIRECTION('ref_axis',(0.,0.,1.));
#8653=DIRECTION('center_axis',(0.,-1.,0.));
#8654=DIRECTION('ref_axis',(1.,0.,0.));
#8655=DIRECTION('center_axis',(0.,-1.,0.));
#8656=DIRECTION('ref_axis',(1.,0.,0.));
#8657=DIRECTION('center_axis',(0.,-1.,0.));
#8658=DIRECTION('ref_axis',(1.,0.,0.));
#8659=DIRECTION('',(0.707106781186547,0.707106781186548,8.65956056235493E-17));
#8660=DIRECTION('center_axis',(0.,-1.,0.));
#8661=DIRECTION('ref_axis',(1.,0.,0.));
#8662=DIRECTION('center_axis',(0.,-1.,0.));
#8663=DIRECTION('ref_axis',(1.,0.,0.));
#8664=DIRECTION('',(0.,1.,0.));
#8665=DIRECTION('center_axis',(0.,1.,0.));
#8666=DIRECTION('ref_axis',(1.,0.,0.));
#8667=DIRECTION('center_axis',(0.,-1.,0.));
#8668=DIRECTION('ref_axis',(1.,0.,0.));
#8669=DIRECTION('',(-0.707106781186547,0.707106781186548,-8.65956056235493E-17));
#8670=DIRECTION('center_axis',(0.,-1.,0.));
#8671=DIRECTION('ref_axis',(0.,0.,-1.));
#8672=DIRECTION('center_axis',(0.,-1.,0.));
#8673=DIRECTION('ref_axis',(1.,0.,0.));
#8674=DIRECTION('center_axis',(0.,1.,0.));
#8675=DIRECTION('ref_axis',(1.,0.,0.));
#8676=DIRECTION('center_axis',(0.,1.,0.));
#8677=DIRECTION('ref_axis',(1.,0.,0.));
#8678=DIRECTION('',(-0.447213595499958,0.894427190999916,-5.47678698264203E-17));
#8679=DIRECTION('center_axis',(0.,-1.,0.));
#8680=DIRECTION('ref_axis',(1.,0.,0.));
#8681=DIRECTION('',(0.,1.,0.));
#8682=DIRECTION('center_axis',(0.866025403784439,0.,-0.5));
#8683=DIRECTION('ref_axis',(0.5,0.,0.866025403784439));
#8684=DIRECTION('',(-0.5,0.,-0.866025403784439));
#8685=DIRECTION('',(0.,-1.,0.));
#8686=DIRECTION('',(0.5,0.,0.866025403784439));
#8687=DIRECTION('',(0.,-1.,0.));
#8688=DIRECTION('center_axis',(1.60246890531964E-16,0.,-1.));
#8689=DIRECTION('ref_axis',(1.,0.,1.60246890531964E-16));
#8690=DIRECTION('',(-1.,0.,-1.60246890531964E-16));
#8691=DIRECTION('',(0.,-1.,0.));
#8692=DIRECTION('',(1.,0.,1.60246890531964E-16));
#8693=DIRECTION('center_axis',(-0.866025403784439,0.,-0.5));
#8694=DIRECTION('ref_axis',(0.5,0.,-0.866025403784439));
#8695=DIRECTION('',(-0.5,0.,0.866025403784439));
#8696=DIRECTION('',(0.,-1.,0.));
#8697=DIRECTION('',(0.5,0.,-0.866025403784439));
#8698=DIRECTION('center_axis',(-0.866025403784439,0.,0.5));
#8699=DIRECTION('ref_axis',(-0.5,0.,-0.866025403784439));
#8700=DIRECTION('',(0.5,0.,0.866025403784439));
#8701=DIRECTION('',(0.,-1.,0.));
#8702=DIRECTION('',(-0.5,0.,-0.866025403784439));
#8703=DIRECTION('center_axis',(-1.60246890531964E-16,0.,1.));
#8704=DIRECTION('ref_axis',(-1.,0.,-1.60246890531964E-16));
#8705=DIRECTION('',(1.,0.,1.60246890531964E-16));
#8706=DIRECTION('',(0.,-1.,0.));
#8707=DIRECTION('',(-1.,0.,-1.60246890531964E-16));
#8708=DIRECTION('center_axis',(0.866025403784439,0.,0.5));
#8709=DIRECTION('ref_axis',(-0.5,0.,0.866025403784439));
#8710=DIRECTION('',(0.5,0.,-0.866025403784439));
#8711=DIRECTION('',(-0.5,0.,0.866025403784439));
#8712=DIRECTION('center_axis',(0.,1.,0.));
#8713=DIRECTION('ref_axis',(1.,0.,0.));
#8714=DIRECTION('center_axis',(0.,-1.,0.));
#8715=DIRECTION('ref_axis',(0.,0.,-1.));
#11670=CARTESIAN_POINT('',(0.,0.,0.));
#11671=CARTESIAN_POINT('Origin',(0.,-0.7,0.));
#11672=CARTESIAN_POINT('',(-0.1954,-0.7,2.39295984553393E-17));
#11673=CARTESIAN_POINT('Origin',(0.,-0.7,0.));
#11674=CARTESIAN_POINT('Origin',(0.3,0.4,0.));
#11675=CARTESIAN_POINT('',(-0.3,0.4,-3.67394039744206E-17));
#11676=CARTESIAN_POINT('Origin',(0.,0.4,0.));
#11677=CARTESIAN_POINT('Origin',(0.,0.375,0.));
#11678=CARTESIAN_POINT('',(-0.35,0.35,-4.28626379701573E-17));
#11679=CARTESIAN_POINT('Origin',(0.,0.35,0.));
#11680=CARTESIAN_POINT('',(-0.325,0.375,-3.9801020972289E-17));
#11681=CARTESIAN_POINT('Origin',(0.,0.19,0.));
#11682=CARTESIAN_POINT('',(-0.35,0.03,-4.28626379701574E-17));
#11683=CARTESIAN_POINT('Origin',(0.,0.03,0.));
#11684=CARTESIAN_POINT('',(-0.35,0.19,-4.28626379701574E-17));
#11685=CARTESIAN_POINT('Origin',(0.,0.0149999999999999,0.));
#11686=CARTESIAN_POINT('',(-0.32,-3.29597460435593E-17,-3.91886975727153E-17));
#11687=CARTESIAN_POINT('Origin',(0.,0.,0.));
#11688=CARTESIAN_POINT('',(-0.335,0.0149999999999999,-4.10256677714363E-17));
#11689=CARTESIAN_POINT('Origin',(0.22,0.,0.));
#11690=CARTESIAN_POINT('',(-0.22,-6.93889390390723E-18,-2.69422295812418E-17));
#11691=CARTESIAN_POINT('Origin',(0.,0.,0.));
#11692=CARTESIAN_POINT('Origin',(0.,-0.02,0.));
#11693=CARTESIAN_POINT('',(-0.1954,-0.0492,2.39295984553393E-17));
#11694=CARTESIAN_POINT('Origin',(0.,-0.0492,0.));
#11695=CARTESIAN_POINT('',(-0.21,-0.02,-2.57175827820944E-17));
#11696=CARTESIAN_POINT('Origin',(0.,-0.8,0.));
#11697=CARTESIAN_POINT('',(-0.1954,-0.8,-2.39295984553393E-17));
#11698=CARTESIAN_POINT('Origin',(0.0866025403784439,-0.4,-0.15));
#11699=CARTESIAN_POINT('',(0.173205080756888,-0.4,0.));
#11700=CARTESIAN_POINT('',(0.0866025403784439,-0.4,-0.15));
#11701=CARTESIAN_POINT('',(0.173205080756888,-0.4,0.));
#11702=CARTESIAN_POINT('',(0.0866025403784439,-0.64,-0.15));
#11703=CARTESIAN_POINT('',(0.0866025403784439,-0.4,-0.15));
#11704=CARTESIAN_POINT('',(0.173205080756888,-0.64,0.));
#11705=CARTESIAN_POINT('',(0.173205080756888,-0.64,0.));
#11706=CARTESIAN_POINT('',(0.173205080756888,-0.4,0.));
#11707=CARTESIAN_POINT('Origin',(-0.0866025403784438,-0.4,-0.15));
#11708=CARTESIAN_POINT('',(-0.0866025403784438,-0.4,-0.15));
#11709=CARTESIAN_POINT('',(0.0866025403784439,-0.4,-0.15));
#11710=CARTESIAN_POINT('',(-0.0866025403784438,-0.64,-0.15));
#11711=CARTESIAN_POINT('',(-0.0866025403784438,-0.4,-0.15));
#11712=CARTESIAN_POINT('',(0.0866025403784439,-0.64,-0.15));
#11713=CARTESIAN_POINT('Origin',(-0.173205080756888,-0.4,-2.77555756156289E-17));
#11714=CARTESIAN_POINT('',(-0.173205080756888,-0.4,-2.12115047744981E-17));
#11715=CARTESIAN_POINT('',(-0.0866025403784438,-0.4,-0.15));
#11716=CARTESIAN_POINT('',(-0.173205080756888,-0.64,-2.77555756156289E-17));
#11717=CARTESIAN_POINT('',(-0.173205080756888,-0.4,-2.12115047744981E-17));
#11718=CARTESIAN_POINT('',(-0.0866025403784438,-0.64,-0.15));
#11719=CARTESIAN_POINT('Origin',(-0.0866025403784439,-0.4,0.15));
#11720=CARTESIAN_POINT('',(-0.0866025403784439,-0.4,0.15));
#11721=CARTESIAN_POINT('',(-0.173205080756888,-0.4,-2.12115047744981E-17));
#11722=CARTESIAN_POINT('',(-0.0866025403784439,-0.64,0.15));
#11723=CARTESIAN_POINT('',(-0.0866025403784439,-0.4,0.15));
#11724=CARTESIAN_POINT('',(-0.173205080756888,-0.64,-2.12115047744981E-17));
#11725=CARTESIAN_POINT('Origin',(0.0866025403784439,-0.4,0.15));
#11726=CARTESIAN_POINT('',(0.0866025403784439,-0.4,0.15));
#11727=CARTESIAN_POINT('',(-0.0866025403784439,-0.4,0.15));
#11728=CARTESIAN_POINT('',(0.0866025403784439,-0.64,0.15));
#11729=CARTESIAN_POINT('',(0.0866025403784439,-0.4,0.15));
#11730=CARTESIAN_POINT('',(-0.0866025403784439,-0.64,0.15));
#11731=CARTESIAN_POINT('Origin',(0.173205080756888,-0.4,0.));
#11732=CARTESIAN_POINT('',(0.0866025403784439,-0.4,0.15));
#11733=CARTESIAN_POINT('',(0.0866025403784439,-0.64,0.15));
#11734=CARTESIAN_POINT('Origin',(0.,-0.4,-2.77555756156289E-17));
#11735=CARTESIAN_POINT('Origin',(0.,-0.64,-2.77555756156289E-17));
#12727=UNCERTAINTY_MEASURE_WITH_UNIT(LENGTH_MEASURE(0.001),#12780,
'DISTANCE_ACCURACY_VALUE',
'Maximum model space distance between geometric entities at asserted c
onnectivities');
#12739=UNCERTAINTY_MEASURE_WITH_UNIT(LENGTH_MEASURE(0.001),#12780,
'DISTANCE_ACCURACY_VALUE',
'Maximum model space distance between geometric entities at asserted c
onnectivities');
#12767=(
GEOMETRIC_REPRESENTATION_CONTEXT(3)
GLOBAL_UNCERTAINTY_ASSIGNED_CONTEXT((#12727))
GLOBAL_UNIT_ASSIGNED_CONTEXT((#12780,#12782,#12783))
REPRESENTATION_CONTEXT('','3D')
);
#12779=(
GEOMETRIC_REPRESENTATION_CONTEXT(3)
GLOBAL_UNCERTAINTY_ASSIGNED_CONTEXT((#12739))
GLOBAL_UNIT_ASSIGNED_CONTEXT((#12780,#12782,#12783))
REPRESENTATION_CONTEXT('','3D')
);
#12780=(
LENGTH_UNIT()
NAMED_UNIT(*)
SI_UNIT(.CENTI.,.METRE.)
);
#12782=(
NAMED_UNIT(*)
PLANE_ANGLE_UNIT()
SI_UNIT($,.RADIAN.)
);
#12783=(
NAMED_UNIT(*)
SI_UNIT($,.STERADIAN.)
SOLID_ANGLE_UNIT()
);
#12811=SHAPE_DEFINITION_REPRESENTATION(#12855,#12950);
#12855=PRODUCT_DEFINITION_SHAPE('',$,#12990);
#12950=SHAPE_REPRESENTATION('',(#7100),#12767);
#12962=PRODUCT_DEFINITION_CONTEXT('part definition',#13081,'design');
#12990=PRODUCT_DEFINITION('M4x7 cap screw','M4x7 cap screw',#13029,#12962);
#13029=PRODUCT_DEFINITION_FORMATION('',$,#13110);
#13081=APPLICATION_CONTEXT(
'Core Data for Automotive Mechanical Design Process');
#13082=PRODUCT_CONTEXT('part definition',#13081,'mechanical');
#13110=PRODUCT('M4x7 cap screw','M4x7 cap screw','M4x7 cap screw',(#13082));
#13185=COLOUR_RGB('Black',0.12,0.14,0.17);
#13186=FILL_AREA_STYLE_COLOUR('',#13185);
#13187=FILL_AREA_STYLE('',(#13186));
#13188=SURFACE_STYLE_FILL_AREA(#13187);
#13189=SURFACE_SIDE_STYLE('',(#13188));
#13190=SURFACE_STYLE_USAGE(.BOTH.,#13189);
#13191=PRESENTATION_STYLE_ASSIGNMENT((#13190));
ENDSEC;
END-ISO-10303-21;
